ISO-10303-21;
HEADER;
/* Generated by software containing ST-Developer
 * from STEP Tools, Inc. (www.steptools.com) 
 */

FILE_DESCRIPTION(
/* description */ ('Turntable on roller ring'),
/* implementation_level */ '2;1');

FILE_NAME(
/* name */ 'Roller tread (3).step',
/* time_stamp */ '2026-10-28T03:23:59-07:00',
/* author */ (''),
/* organization */ (''),
/* preprocessor_version */ 'ST-DEVELOPER v20.2',
/* originating_system */ 'Autodesk Translation Framework v15.17.0.0',
/* authorisation */ '');

FILE_SCHEMA (('AUTOMOTIVE_DESIGN { 1 0 10303 214 3 1 1 }'));
ENDSEC;

DATA;
#10=MECHANICAL_DESIGN_GEOMETRIC_PRESENTATION_REPRESENTATION('',(#673),#16281);
#554=SHAPE_REPRESENTATION_RELATIONSHIP('SRR','None',#16578,#609);
#609=ADVANCED_BREP_SHAPE_REPRESENTATION('',(#741),#16272);
#673=STYLED_ITEM('',(#16925),#741);
#741=MANIFOLD_SOLID_BREP('Body1',#8418);
#975=FACE_BOUND('',#2418,.T.);
#976=FACE_BOUND('',#2420,.T.);
#1227=PLANE('',#10020);
#1228=PLANE('',#10021);
#1692=FACE_OUTER_BOUND('',#2415,.T.);
#1693=FACE_OUTER_BOUND('',#2416,.T.);
#1694=FACE_OUTER_BOUND('',#2417,.T.);
#1695=FACE_OUTER_BOUND('',#2419,.T.);
#2415=EDGE_LOOP('',(#7421,#7422,#7423,#7424));
#2416=EDGE_LOOP('',(#7425,#7426,#7427,#7428));
#2417=EDGE_LOOP('',(#7429));
#2418=EDGE_LOOP('',(#7430));
#2419=EDGE_LOOP('',(#7431));
#2420=EDGE_LOOP('',(#7432));
#2954=LINE('',#15492,#3437);
#2955=LINE('',#15498,#3438);
#3437=VECTOR('',#12613,1.5);
#3438=VECTOR('',#12620,2.);
#3865=CIRCLE('',#10015,1.5);
#3866=CIRCLE('',#10016,1.5);
#3867=CIRCLE('',#10018,2.);
#3868=CIRCLE('',#10019,2.);
#4541=VERTEX_POINT('',#15489);
#4542=VERTEX_POINT('',#15491);
#4543=VERTEX_POINT('',#15495);
#4544=VERTEX_POINT('',#15497);
#5521=EDGE_CURVE('',#4541,#4541,#3865,.T.);
#5522=EDGE_CURVE('',#4541,#4542,#2954,.T.);
#5523=EDGE_CURVE('',#4542,#4542,#3866,.T.);
#5524=EDGE_CURVE('',#4543,#4543,#3867,.T.);
#5525=EDGE_CURVE('',#4543,#4544,#2955,.T.);
#5526=EDGE_CURVE('',#4544,#4544,#3868,.T.);
#7421=ORIENTED_EDGE('',*,*,#5521,.F.);
#7422=ORIENTED_EDGE('',*,*,#5522,.T.);
#7423=ORIENTED_EDGE('',*,*,#5523,.T.);
#7424=ORIENTED_EDGE('',*,*,#5522,.F.);
#7425=ORIENTED_EDGE('',*,*,#5524,.F.);
#7426=ORIENTED_EDGE('',*,*,#5525,.T.);
#7427=ORIENTED_EDGE('',*,*,#5526,.T.);
#7428=ORIENTED_EDGE('',*,*,#5525,.F.);
#7429=ORIENTED_EDGE('',*,*,#5524,.T.);
#7430=ORIENTED_EDGE('',*,*,#5521,.T.);
#7431=ORIENTED_EDGE('',*,*,#5526,.F.);
#7432=ORIENTED_EDGE('',*,*,#5523,.F.);
#7835=CYLINDRICAL_SURFACE('',#10014,1.5);
#7836=CYLINDRICAL_SURFACE('',#10017,2.);
#8295=ADVANCED_FACE('',(#1692),#7835,.F.);
#8296=ADVANCED_FACE('',(#1693),#7836,.T.);
#8297=ADVANCED_FACE('',(#1694,#975),#1227,.T.);
#8298=ADVANCED_FACE('',(#1695,#976),#1228,.F.);
#8418=CLOSED_SHELL('',(#8295,#8296,#8297,#8298));
#10013=AXIS2_PLACEMENT_3D('',#15487,#12607,#12608);
#10014=AXIS2_PLACEMENT_3D('',#15488,#12609,#12610);
#10015=AXIS2_PLACEMENT_3D('',#15490,#12611,#12612);
#10016=AXIS2_PLACEMENT_3D('',#15493,#12614,#12615);
#10017=AXIS2_PLACEMENT_3D('',#15494,#12616,#12617);
#10018=AXIS2_PLACEMENT_3D('',#15496,#12618,#12619);
#10019=AXIS2_PLACEMENT_3D('',#15499,#12621,#12622);
#10020=AXIS2_PLACEMENT_3D('',#15500,#12623,#12624);
#10021=AXIS2_PLACEMENT_3D('',#15501,#12625,#12626);
#12607=DIRECTION('axis',(0.,0.,1.));
#12608=DIRECTION('refdir',(1.,0.,0.));
#12609=DIRECTION('center_axis',(0.,1.,0.));
#12610=DIRECTION('ref_axis',(1.,0.,0.));
#12611=DIRECTION('center_axis',(0.,-1.,0.));
#12612=DIRECTION('ref_axis',(1.,0.,0.));
#12613=DIRECTION('',(0.,-1.,0.));
#12614=DIRECTION('center_axis',(0.,-1.,0.));
#12615=DIRECTION('ref_axis',(1.,0.,0.));
#12616=DIRECTION('center_axis',(0.,1.,0.));
#12617=DIRECTION('ref_axis',(1.,0.,0.));
#12618=DIRECTION('center_axis',(0.,1.,0.));
#12619=DIRECTION('ref_axis',(1.,0.,0.));
#12620=DIRECTION('',(0.,-1.,0.));
#12621=DIRECTION('center_axis',(0.,1.,0.));
#12622=DIRECTION('ref_axis',(1.,0.,0.));
#12623=DIRECTION('center_axis',(0.,1.,0.));
#12624=DIRECTION('ref_axis',(1.,0.,0.));
#12625=DIRECTION('center_axis',(0.,1.,0.));
#12626=DIRECTION('ref_axis',(1.,0.,0.));
#15487=CARTESIAN_POINT('',(0.,0.,0.));
#15488=CARTESIAN_POINT('Origin',(0.,14.35,3.5));
#15489=CARTESIAN_POINT('',(-1.5,15.65,3.5));
#15490=CARTESIAN_POINT('Origin',(0.,15.65,3.5));
#15491=CARTESIAN_POINT('',(-1.5,14.35,3.5));
#15492=CARTESIAN_POINT('',(-1.5,14.35,3.5));
#15493=CARTESIAN_POINT('Origin',(0.,14.35,3.5));
#15494=CARTESIAN_POINT('Origin',(0.,14.35,3.5));
#15495=CARTESIAN_POINT('',(-2.,15.65,3.5));
#15496=CARTESIAN_POINT('Origin',(0.,15.65,3.5));
#15497=CARTESIAN_POINT('',(-2.,14.35,3.5));
#15498=CARTESIAN_POINT('',(-2.,14.35,3.5));
#15499=CARTESIAN_POINT('Origin',(0.,14.35,3.5));
#15500=CARTESIAN_POINT('Origin',(0.,15.65,3.5));
#15501=CARTESIAN_POINT('Origin',(0.,14.35,3.5));
#16203=UNCERTAINTY_MEASURE_WITH_UNIT(LENGTH_MEASURE(0.001),#16282,
'DISTANCE_ACCURACY_VALUE',
'Maximum model space distance between geometric entities at asserted c
onnectivities');
#16212=UNCERTAINTY_MEASURE_WITH_UNIT(LENGTH_MEASURE(0.001),#16282,
'DISTANCE_ACCURACY_VALUE',
'Maximum model space distance between geometric entities at asserted c
onnectivities');
#16272=(
GEOMETRIC_REPRESENTATION_CONTEXT(3)
GLOBAL_UNCERTAINTY_ASSIGNED_CONTEXT((#16203))
GLOBAL_UNIT_ASSIGNED_CONTEXT((#16282,#16284,#16285))
REPRESENTATION_CONTEXT('','3D')
);
#16281=(
GEOMETRIC_REPRESENTATION_CONTEXT(3)
GLOBAL_UNCERTAINTY_ASSIGNED_CONTEXT((#16212))
GLOBAL_UNIT_ASSIGNED_CONTEXT((#16282,#16284,#16285))
REPRESENTATION_CONTEXT('','3D')
);
#16282=(
LENGTH_UNIT()
NAMED_UNIT(*)
SI_UNIT(.CENTI.,.METRE.)
);
#16284=(
NAMED_UNIT(*)
PLANE_ANGLE_UNIT()
SI_UNIT($,.RADIAN.)
);
#16285=(
NAMED_UNIT(*)
SI_UNIT($,.STERADIAN.)
SOLID_ANGLE_UNIT()
);
#16345=SHAPE_DEFINITION_REPRESENTATION(#16479,#16578);
#16479=PRODUCT_DEFINITION_SHAPE('',$,#16647);
#16578=SHAPE_REPRESENTATION('',(#10013),#16272);
#16587=PRODUCT_DEFINITION_CONTEXT('part definition',#16793,'design');
#16647=PRODUCT_DEFINITION('Roller tread (3)','Roller tread (3)',#16715,#16587);
#16715=PRODUCT_DEFINITION_FORMATION('',$,#16854);
#16793=APPLICATION_CONTEXT(
'Core Data for Automotive Mechanical Design Process');
#16794=PRODUCT_CONTEXT('part definition',#16793,'mechanical');
#16854=PRODUCT('Roller tread (3)','Roller tread (3)','Roller tread (3)',(#16794));
#16919=COLOUR_RGB('Sky Blue',0.24,0.69,0.87);
#16920=FILL_AREA_STYLE_COLOUR('',#16919);
#16921=FILL_AREA_STYLE('',(#16920));
#16922=SURFACE_STYLE_FILL_AREA(#16921);
#16923=SURFACE_SIDE_STYLE('',(#16922));
#16924=SURFACE_STYLE_USAGE(.BOTH.,#16923);
#16925=PRESENTATION_STYLE_ASSIGNMENT((#16924));
ENDSEC;
END-ISO-10303-21;
